ISO-10303-21;
HEADER;
/* Generated by software containing ST-Developer
 * from STEP Tools, Inc. (www.steptools.com) 
 */

FILE_DESCRIPTION(
/* description */ ('PAT-122'),
/* implementation_level */ '2;1');

FILE_NAME(
/* name */ 'Cap Screw - M5x20.step',
/* time_stamp */ '2026-10-29T20:20:12-07:00',
/* author */ (''),
/* organization */ (''),
/* preprocessor_version */ 'ST-DEVELOPER v20.2',
/* originating_system */ 'Autodesk Translation Framework v15.17.0.0',
/* authorisation */ '');

FILE_SCHEMA (('AUTOMOTIVE_DESIGN { 1 0 10303 214 3 1 1 }'));
ENDSEC;

DATA;
#10=MECHANICAL_DESIGN_GEOMETRIC_PRESENTATION_REPRESENTATION('',(#507),#10019);
#404=CONICAL_SURFACE('',#6213,0.4,0.785398163397448);
#405=CONICAL_SURFACE('',#6217,0.41,0.785398163397448);
#406=CONICAL_SURFACE('',#6221,0.26,0.463647609000806);
#407=CONICAL_SURFACE('',#6225,0.225,0.785398163397448);
#418=ORIENTED_CLOSED_SHELL('',*,#5631,.F.);
#422=BREP_WITH_VOIDS('Body1',#5630,(#418));
#463=SHAPE_REPRESENTATION_RELATIONSHIP('SRR','None',#10184,#485);
#485=ADVANCED_BREP_SHAPE_REPRESENTATION('',(#422),#10013);
#507=STYLED_ITEM('',(#10355),#422);
#601=FACE_BOUND('',#1410,.T.);
#775=PLANE('',#6211);
#776=PLANE('',#6219);
#777=PLANE('',#6227);
#778=PLANE('',#6228);
#779=PLANE('',#6229);
#780=PLANE('',#6230);
#781=PLANE('',#6231);
#782=PLANE('',#6232);
#783=PLANE('',#6233);
#784=PLANE('',#6234);
#785=PLANE('',#6235);
#1043=FACE_OUTER_BOUND('',#1405,.T.);
#1044=FACE_OUTER_BOUND('',#1406,.T.);
#1045=FACE_OUTER_BOUND('',#1407,.T.);
#1046=FACE_OUTER_BOUND('',#1408,.T.);
#1047=FACE_OUTER_BOUND('',#1409,.T.);
#1048=FACE_OUTER_BOUND('',#1411,.T.);
#1049=FACE_OUTER_BOUND('',#1412,.T.);
#1050=FACE_OUTER_BOUND('',#1413,.T.);
#1051=FACE_OUTER_BOUND('',#1414,.T.);
#1052=FACE_OUTER_BOUND('',#1415,.T.);
#1053=FACE_OUTER_BOUND('',#1416,.T.);
#1054=FACE_OUTER_BOUND('',#1417,.T.);
#1055=FACE_OUTER_BOUND('',#1418,.T.);
#1056=FACE_OUTER_BOUND('',#1419,.T.);
#1057=FACE_OUTER_BOUND('',#1420,.T.);
#1058=FACE_OUTER_BOUND('',#1421,.T.);
#1059=FACE_OUTER_BOUND('',#1422,.T.);
#1405=EDGE_LOOP('',(#4963));
#1406=EDGE_LOOP('',(#4964,#4965,#4966,#4967));
#1407=EDGE_LOOP('',(#4968,#4969,#4970,#4971));
#1408=EDGE_LOOP('',(#4972,#4973,#4974,#4975));
#1409=EDGE_LOOP('',(#4976));
#1410=EDGE_LOOP('',(#4977));
#1411=EDGE_LOOP('',(#4978,#4979,#4980,#4981));
#1412=EDGE_LOOP('',(#4982,#4983,#4984,#4985));
#1413=EDGE_LOOP('',(#4986,#4987,#4988,#4989));
#1414=EDGE_LOOP('',(#4990));
#1415=EDGE_LOOP('',(#4991,#4992,#4993,#4994));
#1416=EDGE_LOOP('',(#4995,#4996,#4997,#4998));
#1417=EDGE_LOOP('',(#4999,#5000,#5001,#5002));
#1418=EDGE_LOOP('',(#5003,#5004,#5005,#5006));
#1419=EDGE_LOOP('',(#5007,#5008,#5009,#5010));
#1420=EDGE_LOOP('',(#5011,#5012,#5013,#5014));
#1421=EDGE_LOOP('',(#5015,#5016,#5017,#5018,#5019,#5020));
#1422=EDGE_LOOP('',(#5021,#5022,#5023,#5024,#5025,#5026));
#1921=LINE('',#9558,#2465);
#1922=LINE('',#9562,#2466);
#1923=LINE('',#9566,#2467);
#1924=LINE('',#9573,#2468);
#1925=LINE('',#9577,#2469);
#1926=LINE('',#9581,#2470);
#1927=LINE('',#9586,#2471);
#1928=LINE('',#9588,#2472);
#1929=LINE('',#9590,#2473);
#1930=LINE('',#9591,#2474);
#1931=LINE('',#9594,#2475);
#1932=LINE('',#9596,#2476);
#1933=LINE('',#9597,#2477);
#1934=LINE('',#9600,#2478);
#1935=LINE('',#9602,#2479);
#1936=LINE('',#9603,#2480);
#1937=LINE('',#9606,#2481);
#1938=LINE('',#9608,#2482);
#1939=LINE('',#9609,#2483);
#1940=LINE('',#9612,#2484);
#1941=LINE('',#9614,#2485);
#1942=LINE('',#9615,#2486);
#1943=LINE('',#9617,#2487);
#1944=LINE('',#9618,#2488);
#2465=VECTOR('',#7526,0.4);
#2466=VECTOR('',#7531,0.425);
#2467=VECTOR('',#7536,0.41);
#2468=VECTOR('',#7545,0.26);
#2469=VECTOR('',#7550,0.25);
#2470=VECTOR('',#7555,0.225);
#2471=VECTOR('',#7560,1.);
#2472=VECTOR('',#7561,1.);
#2473=VECTOR('',#7562,1.);
#2474=VECTOR('',#7563,1.);
#2475=VECTOR('',#7566,1.);
#2476=VECTOR('',#7567,1.);
#2477=VECTOR('',#7568,1.);
#2478=VECTOR('',#7571,1.);
#2479=VECTOR('',#7572,1.);
#2480=VECTOR('',#7573,1.);
#2481=VECTOR('',#7576,1.);
#2482=VECTOR('',#7577,1.);
#2483=VECTOR('',#7578,1.);
#2484=VECTOR('',#7581,1.);
#2485=VECTOR('',#7582,1.);
#2486=VECTOR('',#7583,1.);
#2487=VECTOR('',#7586,1.);
#2488=VECTOR('',#7587,1.);
#2668=CIRCLE('',#6212,0.375);
#2669=CIRCLE('',#6214,0.425);
#2670=CIRCLE('',#6216,0.425);
#2671=CIRCLE('',#6218,0.395);
#2672=CIRCLE('',#6220,0.27);
#2673=CIRCLE('',#6222,0.24505);
#2674=CIRCLE('',#6224,0.24505);
#2675=CIRCLE('',#6226,0.2);
#3072=VERTEX_POINT('',#9553);
#3073=VERTEX_POINT('',#9556);
#3074=VERTEX_POINT('',#9560);
#3075=VERTEX_POINT('',#9564);
#3076=VERTEX_POINT('',#9568);
#3077=VERTEX_POINT('',#9571);
#3078=VERTEX_POINT('',#9575);
#3079=VERTEX_POINT('',#9579);
#3080=VERTEX_POINT('',#9584);
#3081=VERTEX_POINT('',#9585);
#3082=VERTEX_POINT('',#9587);
#3083=VERTEX_POINT('',#9589);
#3084=VERTEX_POINT('',#9593);
#3085=VERTEX_POINT('',#9595);
#3086=VERTEX_POINT('',#9599);
#3087=VERTEX_POINT('',#9601);
#3088=VERTEX_POINT('',#9605);
#3089=VERTEX_POINT('',#9607);
#3090=VERTEX_POINT('',#9611);
#3091=VERTEX_POINT('',#9613);
#3716=EDGE_CURVE('',#3072,#3072,#2668,.T.);
#3717=EDGE_CURVE('',#3073,#3073,#2669,.T.);
#3718=EDGE_CURVE('',#3073,#3072,#1921,.T.);
#3719=EDGE_CURVE('',#3074,#3074,#2670,.T.);
#3720=EDGE_CURVE('',#3074,#3073,#1922,.T.);
#3721=EDGE_CURVE('',#3075,#3075,#2671,.T.);
#3722=EDGE_CURVE('',#3075,#3074,#1923,.T.);
#3723=EDGE_CURVE('',#3076,#3076,#2672,.T.);
#3724=EDGE_CURVE('',#3077,#3077,#2673,.F.);
#3725=EDGE_CURVE('',#3077,#3076,#1924,.T.);
#3726=EDGE_CURVE('',#3078,#3078,#2674,.F.);
#3727=EDGE_CURVE('',#3078,#3077,#1925,.T.);
#3728=EDGE_CURVE('',#3079,#3079,#2675,.T.);
#3729=EDGE_CURVE('',#3079,#3078,#1926,.T.);
#3730=EDGE_CURVE('',#3080,#3081,#1927,.T.);
#3731=EDGE_CURVE('',#3081,#3082,#1928,.T.);
#3732=EDGE_CURVE('',#3082,#3083,#1929,.T.);
#3733=EDGE_CURVE('',#3080,#3083,#1930,.T.);
#3734=EDGE_CURVE('',#3081,#3084,#1931,.T.);
#3735=EDGE_CURVE('',#3084,#3085,#1932,.T.);
#3736=EDGE_CURVE('',#3085,#3082,#1933,.T.);
#3737=EDGE_CURVE('',#3084,#3086,#1934,.T.);
#3738=EDGE_CURVE('',#3086,#3087,#1935,.T.);
#3739=EDGE_CURVE('',#3087,#3085,#1936,.T.);
#3740=EDGE_CURVE('',#3086,#3088,#1937,.T.);
#3741=EDGE_CURVE('',#3088,#3089,#1938,.T.);
#3742=EDGE_CURVE('',#3089,#3087,#1939,.T.);
#3743=EDGE_CURVE('',#3088,#3090,#1940,.T.);
#3744=EDGE_CURVE('',#3090,#3091,#1941,.T.);
#3745=EDGE_CURVE('',#3091,#3089,#1942,.T.);
#3746=EDGE_CURVE('',#3090,#3080,#1943,.T.);
#3747=EDGE_CURVE('',#3083,#3091,#1944,.T.);
#4963=ORIENTED_EDGE('',*,*,#3716,.F.);
#4964=ORIENTED_EDGE('',*,*,#3717,.F.);
#4965=ORIENTED_EDGE('',*,*,#3718,.T.);
#4966=ORIENTED_EDGE('',*,*,#3716,.T.);
#4967=ORIENTED_EDGE('',*,*,#3718,.F.);
#4968=ORIENTED_EDGE('',*,*,#3719,.F.);
#4969=ORIENTED_EDGE('',*,*,#3720,.T.);
#4970=ORIENTED_EDGE('',*,*,#3717,.T.);
#4971=ORIENTED_EDGE('',*,*,#3720,.F.);
#4972=ORIENTED_EDGE('',*,*,#3721,.F.);
#4973=ORIENTED_EDGE('',*,*,#3722,.T.);
#4974=ORIENTED_EDGE('',*,*,#3719,.T.);
#4975=ORIENTED_EDGE('',*,*,#3722,.F.);
#4976=ORIENTED_EDGE('',*,*,#3721,.T.);
#4977=ORIENTED_EDGE('',*,*,#3723,.F.);
#4978=ORIENTED_EDGE('',*,*,#3724,.F.);
#4979=ORIENTED_EDGE('',*,*,#3725,.T.);
#4980=ORIENTED_EDGE('',*,*,#3723,.T.);
#4981=ORIENTED_EDGE('',*,*,#3725,.F.);
#4982=ORIENTED_EDGE('',*,*,#3726,.F.);
#4983=ORIENTED_EDGE('',*,*,#3727,.T.);
#4984=ORIENTED_EDGE('',*,*,#3724,.T.);
#4985=ORIENTED_EDGE('',*,*,#3727,.F.);
#4986=ORIENTED_EDGE('',*,*,#3728,.F.);
#4987=ORIENTED_EDGE('',*,*,#3729,.T.);
#4988=ORIENTED_EDGE('',*,*,#3726,.T.);
#4989=ORIENTED_EDGE('',*,*,#3729,.F.);
#4990=ORIENTED_EDGE('',*,*,#3728,.T.);
#4991=ORIENTED_EDGE('',*,*,#3730,.T.);
#4992=ORIENTED_EDGE('',*,*,#3731,.T.);
#4993=ORIENTED_EDGE('',*,*,#3732,.T.);
#4994=ORIENTED_EDGE('',*,*,#3733,.F.);
#4995=ORIENTED_EDGE('',*,*,#3734,.T.);
#4996=ORIENTED_EDGE('',*,*,#3735,.T.);
#4997=ORIENTED_EDGE('',*,*,#3736,.T.);
#4998=ORIENTED_EDGE('',*,*,#3731,.F.);
#4999=ORIENTED_EDGE('',*,*,#3737,.T.);
#5000=ORIENTED_EDGE('',*,*,#3738,.T.);
#5001=ORIENTED_EDGE('',*,*,#3739,.T.);
#5002=ORIENTED_EDGE('',*,*,#3735,.F.);
#5003=ORIENTED_EDGE('',*,*,#3740,.T.);
#5004=ORIENTED_EDGE('',*,*,#3741,.T.);
#5005=ORIENTED_EDGE('',*,*,#3742,.T.);
#5006=ORIENTED_EDGE('',*,*,#3738,.F.);
#5007=ORIENTED_EDGE('',*,*,#3743,.T.);
#5008=ORIENTED_EDGE('',*,*,#3744,.T.);
#5009=ORIENTED_EDGE('',*,*,#3745,.T.);
#5010=ORIENTED_EDGE('',*,*,#3741,.F.);
#5011=ORIENTED_EDGE('',*,*,#3746,.T.);
#5012=ORIENTED_EDGE('',*,*,#3733,.T.);
#5013=ORIENTED_EDGE('',*,*,#3747,.T.);
#5014=ORIENTED_EDGE('',*,*,#3744,.F.);
#5015=ORIENTED_EDGE('',*,*,#3746,.F.);
#5016=ORIENTED_EDGE('',*,*,#3743,.F.);
#5017=ORIENTED_EDGE('',*,*,#3740,.F.);
#5018=ORIENTED_EDGE('',*,*,#3737,.F.);
#5019=ORIENTED_EDGE('',*,*,#3734,.F.);
#5020=ORIENTED_EDGE('',*,*,#3730,.F.);
#5021=ORIENTED_EDGE('',*,*,#3747,.F.);
#5022=ORIENTED_EDGE('',*,*,#3732,.F.);
#5023=ORIENTED_EDGE('',*,*,#3736,.F.);
#5024=ORIENTED_EDGE('',*,*,#3739,.F.);
#5025=ORIENTED_EDGE('',*,*,#3742,.F.);
#5026=ORIENTED_EDGE('',*,*,#3745,.F.);
#5310=CYLINDRICAL_SURFACE('',#6215,0.425);
#5311=CYLINDRICAL_SURFACE('',#6223,0.24505);
#5539=ADVANCED_FACE('',(#1043),#775,.T.);
#5540=ADVANCED_FACE('',(#1044),#404,.T.);
#5541=ADVANCED_FACE('',(#1045),#5310,.T.);
#5542=ADVANCED_FACE('',(#1046),#405,.T.);
#5543=ADVANCED_FACE('',(#1047,#601),#776,.T.);
#5544=ADVANCED_FACE('',(#1048),#406,.T.);
#5545=ADVANCED_FACE('',(#1049),#5311,.T.);
#5546=ADVANCED_FACE('',(#1050),#407,.T.);
#5547=ADVANCED_FACE('',(#1051),#777,.T.);
#5548=ADVANCED_FACE('',(#1052),#778,.F.);
#5549=ADVANCED_FACE('',(#1053),#779,.F.);
#5550=ADVANCED_FACE('',(#1054),#780,.F.);
#5551=ADVANCED_FACE('',(#1055),#781,.F.);
#5552=ADVANCED_FACE('',(#1056),#782,.F.);
#5553=ADVANCED_FACE('',(#1057),#783,.F.);
#5554=ADVANCED_FACE('',(#1058),#784,.F.);
#5555=ADVANCED_FACE('',(#1059),#785,.F.);
#5630=CLOSED_SHELL('',(#5539,#5540,#5541,#5542,#5543,#5544,#5545,#5546,
#5547));
#5631=CLOSED_SHELL('',(#5548,#5549,#5550,#5551,#5552,#5553,#5554,#5555));
#6210=AXIS2_PLACEMENT_3D('',#9551,#7516,#7517);
#6211=AXIS2_PLACEMENT_3D('',#9552,#7518,#7519);
#6212=AXIS2_PLACEMENT_3D('',#9554,#7520,#7521);
#6213=AXIS2_PLACEMENT_3D('',#9555,#7522,#7523);
#6214=AXIS2_PLACEMENT_3D('',#9557,#7524,#7525);
#6215=AXIS2_PLACEMENT_3D('',#9559,#7527,#7528);
#6216=AXIS2_PLACEMENT_3D('',#9561,#7529,#7530);
#6217=AXIS2_PLACEMENT_3D('',#9563,#7532,#7533);
#6218=AXIS2_PLACEMENT_3D('',#9565,#7534,#7535);
#6219=AXIS2_PLACEMENT_3D('',#9567,#7537,#7538);
#6220=AXIS2_PLACEMENT_3D('',#9569,#7539,#7540);
#6221=AXIS2_PLACEMENT_3D('',#9570,#7541,#7542);
#6222=AXIS2_PLACEMENT_3D('',#9572,#7543,#7544);
#6223=AXIS2_PLACEMENT_3D('',#9574,#7546,#7547);
#6224=AXIS2_PLACEMENT_3D('',#9576,#7548,#7549);
#6225=AXIS2_PLACEMENT_3D('',#9578,#7551,#7552);
#6226=AXIS2_PLACEMENT_3D('',#9580,#7553,#7554);
#6227=AXIS2_PLACEMENT_3D('',#9582,#7556,#7557);
#6228=AXIS2_PLACEMENT_3D('',#9583,#7558,#7559);
#6229=AXIS2_PLACEMENT_3D('',#9592,#7564,#7565);
#6230=AXIS2_PLACEMENT_3D('',#9598,#7569,#7570);
#6231=AXIS2_PLACEMENT_3D('',#9604,#7574,#7575);
#6232=AXIS2_PLACEMENT_3D('',#9610,#7579,#7580);
#6233=AXIS2_PLACEMENT_3D('',#9616,#7584,#7585);
#6234=AXIS2_PLACEMENT_3D('',#9619,#7588,#7589);
#6235=AXIS2_PLACEMENT_3D('',#9620,#7590,#7591);
#7516=DIRECTION('axis',(0.,0.,1.));
#7517=DIRECTION('refdir',(1.,0.,0.));
#7518=DIRECTION('center_axis',(0.,1.,0.));
#7519=DIRECTION('ref_axis',(0.,0.,1.));
#7520=DIRECTION('center_axis',(0.,-1.,0.));
#7521=DIRECTION('ref_axis',(1.,0.,0.));
#7522=DIRECTION('center_axis',(0.,-1.,0.));
#7523=DIRECTION('ref_axis',(1.,0.,0.));
#7524=DIRECTION('center_axis',(0.,-1.,0.));
#7525=DIRECTION('ref_axis',(1.,0.,0.));
#7526=DIRECTION('',(0.707106781186548,0.707106781186547,8.65956056235493E-17));
#7527=DIRECTION('center_axis',(0.,-1.,0.));
#7528=DIRECTION('ref_axis',(1.,0.,0.));
#7529=DIRECTION('center_axis',(0.,-1.,0.));
#7530=DIRECTION('ref_axis',(1.,0.,0.));
#7531=DIRECTION('',(0.,1.,0.));
#7532=DIRECTION('center_axis',(0.,1.,0.));
#7533=DIRECTION('ref_axis',(1.,0.,0.));
#7534=DIRECTION('center_axis',(0.,-1.,0.));
#7535=DIRECTION('ref_axis',(1.,0.,0.));
#7536=DIRECTION('',(-0.707106781186547,0.707106781186548,-8.65956056235493E-17));
#7537=DIRECTION('center_axis',(0.,-1.,0.));
#7538=DIRECTION('ref_axis',(0.,0.,-1.));
#7539=DIRECTION('center_axis',(0.,-1.,0.));
#7540=DIRECTION('ref_axis',(1.,0.,0.));
#7541=DIRECTION('center_axis',(0.,1.,0.));
#7542=DIRECTION('ref_axis',(1.,0.,0.));
#7543=DIRECTION('center_axis',(0.,1.,0.));
#7544=DIRECTION('ref_axis',(1.,0.,0.));
#7545=DIRECTION('',(-0.447213595499958,0.894427190999916,-5.47678698264203E-17));
#7546=DIRECTION('center_axis',(0.,-1.,0.));
#7547=DIRECTION('ref_axis',(1.,0.,0.));
#7548=DIRECTION('center_axis',(0.,1.,0.));
#7549=DIRECTION('ref_axis',(1.,0.,0.));
#7550=DIRECTION('',(0.,1.,0.));
#7551=DIRECTION('center_axis',(0.,1.,0.));
#7552=DIRECTION('ref_axis',(1.,0.,0.));
#7553=DIRECTION('center_axis',(0.,-1.,0.));
#7554=DIRECTION('ref_axis',(1.,0.,0.));
#7555=DIRECTION('',(-0.707106781186547,0.707106781186548,-8.65956056235493E-17));
#7556=DIRECTION('center_axis',(0.,-1.,0.));
#7557=DIRECTION('ref_axis',(0.,0.,-1.));
#7558=DIRECTION('center_axis',(0.866025403784439,0.,-0.5));
#7559=DIRECTION('ref_axis',(0.5,0.,0.866025403784439));
#7560=DIRECTION('',(-0.5,0.,-0.866025403784439));
#7561=DIRECTION('',(0.,-1.,0.));
#7562=DIRECTION('',(0.5,0.,0.866025403784439));
#7563=DIRECTION('',(0.,-1.,0.));
#7564=DIRECTION('center_axis',(1.20185167898973E-16,0.,-1.));
#7565=DIRECTION('ref_axis',(1.,0.,1.20185167898973E-16));
#7566=DIRECTION('',(-1.,0.,-1.20185167898973E-16));
#7567=DIRECTION('',(0.,-1.,0.));
#7568=DIRECTION('',(1.,0.,1.20185167898973E-16));
#7569=DIRECTION('center_axis',(-0.866025403784439,0.,-0.5));
#7570=DIRECTION('ref_axis',(0.5,0.,-0.866025403784439));
#7571=DIRECTION('',(-0.5,0.,0.866025403784439));
#7572=DIRECTION('',(0.,-1.,0.));
#7573=DIRECTION('',(0.5,0.,-0.866025403784439));
#7574=DIRECTION('center_axis',(-0.866025403784439,0.,0.5));
#7575=DIRECTION('ref_axis',(-0.5,0.,-0.866025403784439));
#7576=DIRECTION('',(0.5,0.,0.866025403784439));
#7577=DIRECTION('',(0.,-1.,0.));
#7578=DIRECTION('',(-0.5,0.,-0.866025403784439));
#7579=DIRECTION('center_axis',(-2.40370335797945E-16,0.,1.));
#7580=DIRECTION('ref_axis',(-1.,0.,-2.40370335797945E-16));
#7581=DIRECTION('',(1.,0.,2.40370335797945E-16));
#7582=DIRECTION('',(0.,-1.,0.));
#7583=DIRECTION('',(-1.,0.,-2.40370335797945E-16));
#7584=DIRECTION('center_axis',(0.866025403784439,0.,0.5));
#7585=DIRECTION('ref_axis',(-0.5,0.,0.866025403784439));
#7586=DIRECTION('',(0.5,0.,-0.866025403784439));
#7587=DIRECTION('',(-0.5,0.,0.866025403784439));
#7588=DIRECTION('center_axis',(0.,1.,0.));
#7589=DIRECTION('ref_axis',(1.,0.,0.));
#7590=DIRECTION('center_axis',(0.,-1.,0.));
#7591=DIRECTION('ref_axis',(0.,0.,-1.));
#9551=CARTESIAN_POINT('',(0.,0.,0.));
#9552=CARTESIAN_POINT('Origin',(0.375,0.5,0.));
#9553=CARTESIAN_POINT('',(-0.375,0.5,-4.59242549680257E-17));
#9554=CARTESIAN_POINT('Origin',(0.,0.5,0.));
#9555=CARTESIAN_POINT('Origin',(0.,0.475,0.));
#9556=CARTESIAN_POINT('',(-0.425,0.45,-5.20474889637625E-17));
#9557=CARTESIAN_POINT('Origin',(0.,0.45,0.));
#9558=CARTESIAN_POINT('',(-0.4,0.475,-4.89858719658941E-17));
#9559=CARTESIAN_POINT('Origin',(0.,0.24,0.));
#9560=CARTESIAN_POINT('',(-0.425,0.0299999999999998,-5.20474889637625E-17));
#9561=CARTESIAN_POINT('Origin',(0.,0.0299999999999998,0.));
#9562=CARTESIAN_POINT('',(-0.425,0.24,-5.20474889637625E-17));
#9563=CARTESIAN_POINT('Origin',(0.,0.0150000000000001,0.));
#9564=CARTESIAN_POINT('',(-0.395,4.85722573273506E-17,-4.83735485663204E-17));
#9565=CARTESIAN_POINT('Origin',(0.,0.,0.));
#9566=CARTESIAN_POINT('',(-0.41,0.0150000000000001,-5.02105187650415E-17));
#9567=CARTESIAN_POINT('Origin',(0.27,0.,0.));
#9568=CARTESIAN_POINT('',(-0.27,0.,-3.30654635769785E-17));
#9569=CARTESIAN_POINT('Origin',(0.,0.,0.));
#9570=CARTESIAN_POINT('Origin',(0.,-0.02,0.));
#9571=CARTESIAN_POINT('',(-0.24505,-0.0498999999999999,3.00099698131059E-17));
#9572=CARTESIAN_POINT('Origin',(0.,-0.0498999999999999,0.));
#9573=CARTESIAN_POINT('',(-0.26,-0.02,-3.18408167778312E-17));
#9574=CARTESIAN_POINT('Origin',(0.,-0.995,0.));
#9575=CARTESIAN_POINT('',(-0.24505,-1.95495,3.00099698131059E-17));
#9576=CARTESIAN_POINT('Origin',(0.,-1.95495,0.));
#9577=CARTESIAN_POINT('',(-0.24505,-0.995,-3.00099698131059E-17));
#9578=CARTESIAN_POINT('Origin',(0.,-1.975,0.));
#9579=CARTESIAN_POINT('',(-0.2,-2.,-2.44929359829471E-17));
#9580=CARTESIAN_POINT('Origin',(0.,-2.,0.));
#9581=CARTESIAN_POINT('',(-0.225,-1.975,-2.75545529808154E-17));
#9582=CARTESIAN_POINT('Origin',(0.,-2.,0.));
#9583=CARTESIAN_POINT('Origin',(0.115470053837925,-0.5,-0.2));
#9584=CARTESIAN_POINT('',(0.23094010767585,-0.5,0.));
#9585=CARTESIAN_POINT('',(0.115470053837925,-0.5,-0.2));
#9586=CARTESIAN_POINT('',(0.23094010767585,-0.5,0.));
#9587=CARTESIAN_POINT('',(0.115470053837925,-0.8,-0.2));
#9588=CARTESIAN_POINT('',(0.115470053837925,-0.5,-0.2));
#9589=CARTESIAN_POINT('',(0.23094010767585,-0.8,0.));
#9590=CARTESIAN_POINT('',(0.23094010767585,-0.8,0.));
#9591=CARTESIAN_POINT('',(0.23094010767585,-0.5,0.));
#9592=CARTESIAN_POINT('Origin',(-0.115470053837925,-0.5,-0.2));
#9593=CARTESIAN_POINT('',(-0.115470053837925,-0.5,-0.2));
#9594=CARTESIAN_POINT('',(0.115470053837925,-0.5,-0.2));
#9595=CARTESIAN_POINT('',(-0.115470053837925,-0.8,-0.2));
#9596=CARTESIAN_POINT('',(-0.115470053837925,-0.5,-0.2));
#9597=CARTESIAN_POINT('',(0.115470053837925,-0.8,-0.2));
#9598=CARTESIAN_POINT('Origin',(-0.23094010767585,-0.5,-2.77555756156289E-17));
#9599=CARTESIAN_POINT('',(-0.23094010767585,-0.5,-2.82820063659975E-17));
#9600=CARTESIAN_POINT('',(-0.115470053837925,-0.5,-0.2));
#9601=CARTESIAN_POINT('',(-0.23094010767585,-0.8,-2.77555756156289E-17));
#9602=CARTESIAN_POINT('',(-0.23094010767585,-0.5,-2.82820063659975E-17));
#9603=CARTESIAN_POINT('',(-0.115470053837925,-0.8,-0.2));
#9604=CARTESIAN_POINT('Origin',(-0.115470053837925,-0.5,0.2));
#9605=CARTESIAN_POINT('',(-0.115470053837925,-0.5,0.2));
#9606=CARTESIAN_POINT('',(-0.23094010767585,-0.5,-2.82820063659975E-17));
#9607=CARTESIAN_POINT('',(-0.115470053837925,-0.8,0.2));
#9608=CARTESIAN_POINT('',(-0.115470053837925,-0.5,0.2));
#9609=CARTESIAN_POINT('',(-0.23094010767585,-0.8,-2.82820063659975E-17));
#9610=CARTESIAN_POINT('Origin',(0.115470053837925,-0.5,0.2));
#9611=CARTESIAN_POINT('',(0.115470053837925,-0.5,0.2));
#9612=CARTESIAN_POINT('',(-0.115470053837925,-0.5,0.2));
#9613=CARTESIAN_POINT('',(0.115470053837925,-0.8,0.2));
#9614=CARTESIAN_POINT('',(0.115470053837925,-0.5,0.2));
#9615=CARTESIAN_POINT('',(-0.115470053837925,-0.8,0.2));
#9616=CARTESIAN_POINT('Origin',(0.23094010767585,-0.5,0.));
#9617=CARTESIAN_POINT('',(0.115470053837925,-0.5,0.2));
#9618=CARTESIAN_POINT('',(0.115470053837925,-0.8,0.2));
#9619=CARTESIAN_POINT('Origin',(0.,-0.5,0.));
#9620=CARTESIAN_POINT('Origin',(0.,-0.8,0.));
#9989=UNCERTAINTY_MEASURE_WITH_UNIT(LENGTH_MEASURE(0.001),#10020,
'DISTANCE_ACCURACY_VALUE',
'Maximum model space distance between geometric entities at asserted c
onnectivities');
#9995=UNCERTAINTY_MEASURE_WITH_UNIT(LENGTH_MEASURE(0.001),#10020,
'DISTANCE_ACCURACY_VALUE',
'Maximum model space distance between geometric entities at asserted c
onnectivities');
#10013=(
GEOMETRIC_REPRESENTATION_CONTEXT(3)
GLOBAL_UNCERTAINTY_ASSIGNED_CONTEXT((#9989))
GLOBAL_UNIT_ASSIGNED_CONTEXT((#10020,#10022,#10023))
REPRESENTATION_CONTEXT('','3D')
);
#10019=(
GEOMETRIC_REPRESENTATION_CONTEXT(3)
GLOBAL_UNCERTAINTY_ASSIGNED_CONTEXT((#9995))
GLOBAL_UNIT_ASSIGNED_CONTEXT((#10020,#10022,#10023))
REPRESENTATION_CONTEXT('','3D')
);
#10020=(
LENGTH_UNIT()
NAMED_UNIT(*)
SI_UNIT(.CENTI.,.METRE.)
);
#10022=(
NAMED_UNIT(*)
PLANE_ANGLE_UNIT()
SI_UNIT($,.RADIAN.)
);
#10023=(
NAMED_UNIT(*)
SI_UNIT($,.STERADIAN.)
SOLID_ANGLE_UNIT()
);
#10041=SHAPE_DEFINITION_REPRESENTATION(#10064,#10184);
#10064=PRODUCT_DEFINITION_SHAPE('',$,#10208);
#10184=SHAPE_REPRESENTATION('',(#6210),#10013);
#10190=PRODUCT_DEFINITION_CONTEXT('part definition',#10261,'design');
#10208=PRODUCT_DEFINITION('Cap Screw - M5x20','Cap Screw - M5x20',
#10231,#10190);
#10231=PRODUCT_DEFINITION_FORMATION('',$,#10280);
#10261=APPLICATION_CONTEXT(
'Core Data for Automotive Mechanical Design Process');
#10262=PRODUCT_CONTEXT('part definition',#10261,'mechanical');
#10280=PRODUCT('Cap Screw - M5x20','Cap Screw - M5x20',
'Cap Screw - M5x20',(#10262));
#10349=COLOUR_RGB('Black',0.12,0.14,0.17);
#10350=FILL_AREA_STYLE_COLOUR('',#10349);
#10351=FILL_AREA_STYLE('',(#10350));
#10352=SURFACE_STYLE_FILL_AREA(#10351);
#10353=SURFACE_SIDE_STYLE('',(#10352));
#10354=SURFACE_STYLE_USAGE(.BOTH.,#10353);
#10355=PRESENTATION_STYLE_ASSIGNMENT((#10354));
ENDSEC;
END-ISO-10303-21;
